ISO-10303-21;
HEADER;
FILE_DESCRIPTION (('STEP AP214'),
    '1' );
FILE_NAME ('socket head cap screw_iso_ISO 4762 M5 x 12 - 12N.step',
    '2026-10-24T13:33:06',
    ( '' ),
    ( '' ),
    'SwSTEP 2.0',
    'SolidWorks 2026',
    '' );
FILE_SCHEMA (( 'AUTOMOTIVE_DESIGN' ));
ENDSEC;

DATA;
#18=MECHANICAL_DESIGN_GEOMETRIC_PRESENTATION_REPRESENTATION('',(#6765),#7674);
#61=DIRECTION ( 'NONE',  ( -1.000000000000000000, -0.000000000000000000, -0.000000000000000000 ) ) ;
#83=AXIS2_PLACEMENT_3D ( 'NONE', #9067, #7962, #321 ) ;
#93=CARTESIAN_POINT ( 'NONE',  ( 2.500000000000000000, 2.357898499370433054, -1.951563910473907981E-15 ) ) ;
#125=AXIS2_PLACEMENT_3D ( 'NONE', #612, #5076, #9487 ) ;
#128=AXIS2_PLACEMENT_3D ( 'NONE', #6258, #5252, #1681 ) ;
#145=VERTEX_POINT ( 'NONE', #3075 ) ;
#155=EDGE_LOOP ( 'NONE', ( #7067, #11901, #14288, #9379, #2172, #12925 ) ) ;
#160=CARTESIAN_POINT ( 'NONE',  ( 2.500000000000000000, -1.178949249685218303, -2.041999999999998039 ) ) ;
#216=CYLINDRICAL_SURFACE ( 'NONE', #14049, 4.250000000000000000 ) ;
#226=EDGE_LOOP ( 'NONE', ( #6646, #8713, #11419, #2781 ) ) ;
#247=VERTEX_POINT ( 'NONE', #2541 ) ;
#264=CIRCLE ( 'NONE', #6784, 2.500000000000000444 ) ;
#272=ORIENTED_EDGE ( 'NONE', *, *, #4554, .T. ) ;
#273=ADVANCED_FACE ( 'NONE', ( #9135 ), #3628, .F. ) ;
#278=VERTEX_POINT ( 'NONE', #12335 ) ;
#294=ORIENTED_EDGE ( 'NONE', *, *, #6857, .T. ) ;
#297=DIRECTION ( 'NONE',  ( -0.000000000000000000, 0.8660254037844390407, 0.4999999999999993339 ) ) ;
#307=FACE_OUTER_BOUND ( 'NONE', #226, .T. ) ;
#313=( NAMED_UNIT ( * ) SI_UNIT ( $, .STERADIAN. ) SOLID_ANGLE_UNIT ( ) );
#321=DIRECTION ( 'NONE',  ( 0.000000000000000000, 0.000000000000000000, -1.000000000000000000 ) ) ;
#329=CARTESIAN_POINT ( 'NONE',  ( 2.500000000000000000, -1.768423874527823569, 1.021000000000002794 ) ) ;
#387=CARTESIAN_POINT ( 'NONE',  ( 2.500000000000000000, -2.357898499370432610, 3.252606517456513302E-15 ) ) ;
#395=ORIENTED_EDGE ( 'NONE', *, *, #13834, .T. ) ;
#401=ORIENTED_EDGE ( 'NONE', *, *, #3300, .T. ) ;
#428=CARTESIAN_POINT ( 'NONE',  ( 0.000000000000000000, 1.178949249685218525, 2.041999999999999371 ) ) ;
#440=VECTOR ( 'NONE', #5647, 1000.000000000000000 ) ;
#482=ORIENTED_EDGE ( 'NONE', *, *, #7284, .T. ) ;
#492=VECTOR ( 'NONE', #6472, 1000.000000000000114 ) ;
#502=DIRECTION ( 'NONE',  ( -1.000000000000000000, 0.000000000000000000, -0.000000000000000000 ) ) ;
#506=ADVANCED_FACE ( 'NONE', ( #12686 ), #13842, .F. ) ;
#518=CARTESIAN_POINT ( 'NONE',  ( 2.500000000000000000, 2.357898499370433054, -1.951563910473907981E-15 ) ) ;
#522=CARTESIAN_POINT ( 'NONE',  ( 2.500000000000000000, -1.178949249685218303, -2.041999999999998039 ) ) ;
#535=DIRECTION ( 'NONE',  ( 0.000000000000000000, 0.000000000000000000, -1.000000000000000000 ) ) ;
#561=DIRECTION ( 'NONE',  ( -1.000000000000000000, -0.000000000000000000, -0.000000000000000000 ) ) ;
#565=AXIS2_PLACEMENT_3D ( 'NONE', #12068, #10768, #6552 ) ;
#568=VERTEX_POINT ( 'NONE', #766 ) ;
#589=ORIENTED_EDGE ( 'NONE', *, *, #5616, .T. ) ;
#597=DIRECTION ( 'NONE',  ( -1.000000000000000000, -0.000000000000000000, -0.000000000000000000 ) ) ;
#612=CARTESIAN_POINT ( 'NONE',  ( 2.500000000000000000, 2.357898499370433054, -1.951563910473907981E-15 ) ) ;
#673=PLANE ( 'NONE',  #8840 ) ;
#683=DIRECTION ( 'NONE',  ( -0.7071067811865369146, 8.659560562355062281E-17, -0.7071067811865582309 ) ) ;
#707=ORIENTED_EDGE ( 'NONE', *, *, #13975, .F. ) ;
#766=CARTESIAN_POINT ( 'NONE',  ( 0.000000000000000000, -2.357898499370432610, 3.252606517456513302E-15 ) ) ;
#779=CARTESIAN_POINT ( 'NONE',  ( 5.000000000000004441, 0.000000000000000000, 0.000000000000000000 ) ) ;
#794=VERTEX_POINT ( 'NONE', #5644 ) ;
#814=DIRECTION ( 'NONE',  ( 0.000000000000000000, -1.287488025362403787E-15, -1.000000000000000000 ) ) ;
#819=CIRCLE ( 'NONE', #9878, 4.000000000000000000 ) ;
#850=DIRECTION ( 'NONE',  ( 0.000000000000000000, 0.000000000000000000, 1.000000000000000000 ) ) ;
#853=ADVANCED_FACE ( 'NONE', ( #8980 ), #9496, .T. ) ;
#895=PLANE ( 'NONE',  #11592 ) ;
#896=EDGE_CURVE ( 'NONE', #1984, #11681, #9189, .T. ) ;
#901=CARTESIAN_POINT ( 'NONE',  ( 5.200000000000002842, 0.000000000000000000, 0.000000000000000000 ) ) ;
#959=LINE ( 'NONE', #7723, #4871 ) ;
#973=ORIENTED_EDGE ( 'NONE', *, *, #5876, .T. ) ;
#1026=CARTESIAN_POINT ( 'NONE',  ( 2.500000000000000000, 2.357898499370433054, -1.951563910473907981E-15 ) ) ;
#1055=ADVANCED_FACE ( 'NONE', ( #8538 ), #2001, .T. ) ;
#1064=EDGE_CURVE ( 'NONE', #10103, #13709, #11359, .T. ) ;
#1078=ADVANCED_FACE ( 'NONE', ( #3255 ), #895, .T. ) ;
#1081=ORIENTED_EDGE ( 'NONE', *, *, #2069, .F. ) ;
#1088=CARTESIAN_POINT ( 'NONE',  ( 2.500000000000000000, 1.178949249685218525, 2.041999999999999371 ) ) ;
#1153=CARTESIAN_POINT ( 'NONE',  ( 2.500000000000000000, -1.178949249685213863, 2.042000000000002924 ) ) ;
#1188=VERTEX_POINT ( 'NONE', #3330 ) ;
#1207=ORIENTED_EDGE ( 'NONE', *, *, #11435, .T. ) ;
#1208=CARTESIAN_POINT ( 'NONE',  ( 0.000000000000000000, -1.178949249685213863, 2.042000000000002924 ) ) ;
#1223=ORIENTED_EDGE ( 'NONE', *, *, #9152, .T. ) ;
#1235=PLANE ( 'NONE',  #9389 ) ;
#1283=AXIS2_PLACEMENT_3D ( 'NONE', #3071, #1894, #4292 ) ;
#1289=ORIENTED_EDGE ( 'NONE', *, *, #7359, .T. ) ;
#1298=VERTEX_POINT ( 'NONE', #10465 ) ;
#1319=ORIENTED_EDGE ( 'NONE', *, *, #9416, .T. ) ;
#1340=FACE_OUTER_BOUND ( 'NONE', #8047, .T. ) ;
#1342=EDGE_CURVE ( 'NONE', #568, #2622, #13004, .T. ) ;
#1357=VECTOR ( 'NONE', #4551, 1000.000000000000114 ) ;
#1392=LINE ( 'NONE', #3871, #9220 ) ;
#1402=AXIS2_PLACEMENT_3D ( 'NONE', #12026, #2967, #14188 ) ;
#1419=ORIENTED_EDGE ( 'NONE', *, *, #9116, .T. ) ;
#1428=EDGE_CURVE ( 'NONE', #11776, #12690, #14223, .T. ) ;
#1457=ORIENTED_EDGE ( 'NONE', *, *, #13975, .T. ) ;
#1481=DIRECTION ( 'NONE',  ( 0.000000000000000000, 0.000000000000000000, 1.000000000000000000 ) ) ;
#1484=EDGE_LOOP ( 'NONE', ( #13326, #12481 ) ) ;
#1523=ORIENTED_EDGE ( 'NONE', *, *, #8262, .F. ) ;
#1548=CONICAL_SURFACE ( 'NONE', #12457, 2.055000000000000160, 0.7853981633974633780 ) ;
#1561=DIRECTION ( 'NONE',  ( 1.000000000000000000, 0.000000000000000000, 0.000000000000000000 ) ) ;
#1588=UNCERTAINTY_MEASURE_WITH_UNIT (LENGTH_MEASURE( 1.000000000000000082E-05 ), #2896, 'distance_accuracy_value', 'NONE');
#1599=PRODUCT_DEFINITION ( 'UNKNOWN', '', #12106, #8270 ) ;
#1612=AXIS2_PLACEMENT_3D ( 'NONE', #11512, #8386, #13754 ) ;
#1617=CARTESIAN_POINT ( 'NONE',  ( 0.2500000000000002220, 0.000000000000000000, 0.000000000000000000 ) ) ;
#1625=VERTEX_POINT ( 'NONE', #6894 ) ;
#1640=CARTESIAN_POINT ( 'NONE',  ( 2.500000000000000000, 0.000000000000000000, 0.000000000000000000 ) ) ;
#1681=DIRECTION ( 'NONE',  ( 0.000000000000000000, -1.224646799147353454E-16, 1.000000000000000000 ) ) ;
#1716=CARTESIAN_POINT ( 'NONE',  ( 17.00000000000000000, 2.789133085058097101E-16, -2.055000000000000160 ) ) ;
#1719=SURFACE_STYLE_FILL_AREA ( #9641 ) ;
#1738=DIRECTION ( 'NONE',  ( 0.000000000000000000, 0.000000000000000000, -1.000000000000000000 ) ) ;
#1763=DIRECTION ( 'NONE',  ( 0.000000000000000000, -1.000000000000000000, 1.471414886128461471E-15 ) ) ;
#1774=EDGE_CURVE ( 'NONE', #1625, #278, #2983, .T. ) ;
#1778=VECTOR ( 'NONE', #10166, 999.9999999999998863 ) ;
#1783=DIRECTION ( 'NONE',  ( -1.000000000000000000, -0.000000000000000000, -0.000000000000000000 ) ) ;
#1787=VECTOR ( 'NONE', #4780, 1000.000000000000000 ) ;
#1811=LINE ( 'NONE', #9801, #6630 ) ;
#1816=DIRECTION ( 'NONE',  ( 0.000000000000000000, 0.000000000000000000, 1.000000000000000000 ) ) ;
#1830=ORIENTED_EDGE ( 'NONE', *, *, #13625, .T. ) ;
#1841=ORIENTED_EDGE ( 'NONE', *, *, #3449, .T. ) ;
#1853=DIRECTION ( 'NONE',  ( 0.000000000000000000, -1.000000000000000000, 1.287488025362403787E-15 ) ) ;
#1860=DIRECTION ( 'NONE',  ( 0.000000000000000000, 0.000000000000000000, 1.000000000000000000 ) ) ;
#1872=VERTEX_POINT ( 'NONE', #11824 ) ;
#1890=DIRECTION ( 'NONE',  ( -1.000000000000000000, -0.000000000000000000, -0.000000000000000000 ) ) ;
#1894=DIRECTION ( 'NONE',  ( 0.000000000000000000, -1.000000000000000000, 0.000000000000000000 ) ) ;
#1941=( NAMED_UNIT ( * ) PLANE_ANGLE_UNIT ( ) SI_UNIT ( $, .RADIAN. ) );
#1984=VERTEX_POINT ( 'NONE', #5506 ) ;
#2001=CYLINDRICAL_SURFACE ( 'NONE', #4420, 2.500000000000000444 ) ;
#2032=CARTESIAN_POINT ( 'NONE',  ( 5.000000000000000888, 4.250000000000000000, 0.000000000000000000 ) ) ;
#2069=EDGE_CURVE ( 'NONE', #8138, #8017, #7226, .T. ) ;
#2084=DIRECTION ( 'NONE',  ( 1.000000000000000000, 0.000000000000000000, 0.000000000000000000 ) ) ;
#2090=CONICAL_SURFACE ( 'NONE', #10199, 2.041999999999999815, 1.047197551196591858 ) ;
#2097=EDGE_LOOP ( 'NONE', ( #12891, #12875, #7619, #9143 ) ) ;
#2100=DIRECTION ( 'NONE',  ( 0.000000000000000000, 1.224646799147353207E-16, 1.000000000000000000 ) ) ;
#2143=DIRECTION ( 'NONE',  ( 1.000000000000000000, 0.000000000000000000, 0.000000000000000000 ) ) ;
#2146=LINE ( 'NONE', #8746, #11857 ) ;
#2168=EDGE_LOOP ( 'NONE', ( #5649, #1457, #10994 ) ) ;
#2172=ORIENTED_EDGE ( 'NONE', *, *, #10401, .F. ) ;
#2184=EDGE_LOOP ( 'NONE', ( #7998, #13015, #10265, #7876 ) ) ;
#2235=EDGE_LOOP ( 'NONE', ( #7959, #3337, #5658, #10144, #1419 ) ) ;
#2256=AXIS2_PLACEMENT_3D ( 'NONE', #11705, #8430, #7495 ) ;
#2273=MECHANICAL_DESIGN_GEOMETRIC_PRESENTATION_REPRESENTATION('',(#5478),#12889);
#2288=CARTESIAN_POINT ( 'NONE',  ( 2.500000000000000000, 2.357898499370433054, -1.951563910473907981E-15 ) ) ;
#2295=VECTOR ( 'NONE', #4438, 999.9999999999998863 ) ;
#2311=ORIENTED_EDGE ( 'NONE', *, *, #8590, .F. ) ;
#2324=CARTESIAN_POINT ( 'NONE',  ( 5.000000000000002665, 3.306546357697854226E-16, 2.700000000000000622 ) ) ;
#2350=ORIENTED_EDGE ( 'NONE', *, *, #13834, .F. ) ;
#2377=DIRECTION ( 'NONE',  ( 1.000000000000000000, 0.000000000000000000, 0.000000000000000000 ) ) ;
#2393=CARTESIAN_POINT ( 'NONE',  ( 0.000000000000000000, -1.178949249685213863, 2.042000000000002924 ) ) ;
#2407=PRODUCT ( 'socket head cap screw_iso_ISO 4762 M5 x 12 - 12N', 'socket head cap screw_iso_ISO 4762 M5 x 12 - 12N', '', ( #3177 ) ) ;
#2428=CARTESIAN_POINT ( 'NONE',  ( 2.500000000000000000, 0.000000000000000000, 0.000000000000000000 ) ) ;
#2459=VECTOR ( 'NONE', #5445, 1000.000000000000114 ) ;
#2467=ADVANCED_FACE ( 'NONE', ( #6699 ), #1235, .F. ) ;
#2478=CARTESIAN_POINT ( 'NONE',  ( 2.500000000000000000, 1.178949249685213863, -2.042000000000001148 ) ) ;
#2496=CARTESIAN_POINT ( 'NONE',  ( 0.000000000000000000, 0.000000000000000000, 0.000000000000000000 ) ) ;
#2541=CARTESIAN_POINT ( 'NONE',  ( 0.2500000000000002220, 0.000000000000000000, 4.250000000000000000 ) ) ;
#2554=CARTESIAN_POINT ( 'NONE',  ( 5.200000000000002842, 0.000000000000000000, 2.500000000000000444 ) ) ;
#2622=VERTEX_POINT ( 'NONE', #13561 ) ;
#2634=ORIENTED_EDGE ( 'NONE', *, *, #10400, .T. ) ;
#2639=FACE_OUTER_BOUND ( 'NONE', #3974, .T. ) ;
#2656=LINE ( 'NONE', #11367, #6007 ) ;
#2704=ORIENTED_EDGE ( 'NONE', *, *, #8884, .T. ) ;
#2732=CARTESIAN_POINT ( 'NONE',  ( 2.500000000000000000, -2.357898499370432610, 3.252606517456513302E-15 ) ) ;
#2745=ADVANCED_FACE ( 'NONE', ( #7407 ), #7327, .F. ) ;
#2758=EDGE_CURVE ( 'NONE', #9311, #4062, #10893, .T. ) ;
#2781=ORIENTED_EDGE ( 'NONE', *, *, #5876, .F. ) ;
#2782=VECTOR ( 'NONE', #11727, 1000.000000000000000 ) ;
#2789=CARTESIAN_POINT ( 'NONE',  ( 2.500000000000000000, -1.178949249685213863, 2.042000000000002924 ) ) ;
#2798=PLANE ( 'NONE',  #9100 ) ;
#2818=EDGE_CURVE ( 'NONE', #1984, #1298, #6785, .T. ) ;
#2830=DIRECTION ( 'NONE',  ( 0.000000000000000000, 0.000000000000000000, -1.000000000000000000 ) ) ;
#2861=VERTEX_POINT ( 'NONE', #9660 ) ;
#2878=EDGE_CURVE ( 'NONE', #1188, #10103, #3668, .T. ) ;
#2896=( LENGTH_UNIT ( ) NAMED_UNIT ( * ) SI_UNIT ( .MILLI., .METRE. ) );
#2933=CARTESIAN_POINT ( 'NONE',  ( 0.2500000000000002220, 0.000000000000000000, 0.000000000000000000 ) ) ;
#2943=DIRECTION ( 'NONE',  ( -0.000000000000000000, 1.471414886128461471E-15, 1.000000000000000000 ) ) ;
#2953=PLANE ( 'NONE',  #5825 ) ;
#2957=VECTOR ( 'NONE', #11401, 1000.000000000000114 ) ;
#2967=DIRECTION ( 'NONE',  ( -1.000000000000000000, -0.000000000000000000, -0.000000000000000000 ) ) ;
#2983=LINE ( 'NONE', #7252, #11418 ) ;
#2989=ORIENTED_EDGE ( 'NONE', *, *, #896, .F. ) ;
#3014=AXIS2_PLACEMENT_3D ( 'NONE', #7870, #2377, #11013 ) ;
#3041=DIRECTION ( 'NONE',  ( 0.000000000000000000, -0.5000000000000011102, -0.8660254037844379305 ) ) ;
#3071=CARTESIAN_POINT ( 'NONE',  ( 5.200000000000002842, 0.000000000000000000, -2.700000000000000622 ) ) ;
#3075=CARTESIAN_POINT ( 'NONE',  ( 2.500000000000000000, 3.004629197474318851E-15, 2.042000000000000259 ) ) ;
#3130=DIRECTION ( 'NONE',  ( 0.000000000000000000, 0.000000000000000000, 1.000000000000000000 ) ) ;
#3137=DIRECTION ( 'NONE',  ( 0.000000000000000000, 0.000000000000000000, 1.000000000000000000 ) ) ;
#3140=PLANE ( 'NONE',  #9746 ) ;
#3175=CIRCLE ( 'NONE', #11270, 4.000000000000000000 ) ;
#3177=PRODUCT_CONTEXT ( 'NONE', #4616, 'mechanical' ) ;
#3201=CARTESIAN_POINT ( 'NONE',  ( 16.55500000000001393, 3.061616997868383634E-16, -2.500000000000000444 ) ) ;
#3207=CIRCLE ( 'NONE', #12914, 2.041999999999999815 ) ;
#3255=FACE_OUTER_BOUND ( 'NONE', #5659, .T. ) ;
#3300=EDGE_CURVE ( 'NONE', #13189, #13709, #7162, .T. ) ;
#3302=COLOUR_RGB ( '',1.000000000000000000, 0.9490196078431372140, 0.9098039215686274384 ) ;
#3306=VERTEX_POINT ( 'NONE', #1716 ) ;
#3319=VECTOR ( 'NONE', #9421, 1000.000000000000000 ) ;
#3330=CARTESIAN_POINT ( 'NONE',  ( 2.500000000000000000, 1.768423874527824902, 1.020999999999999019 ) ) ;
#3337=ORIENTED_EDGE ( 'NONE', *, *, #14276, .F. ) ;
#3341=LINE ( 'NONE', #93, #1357 ) ;
#3358=LINE ( 'NONE', #6606, #2295 ) ;
#3393=ADVANCED_FACE ( 'NONE', ( #8955 ), #2090, .F. ) ;
#3398=CARTESIAN_POINT ( 'NONE',  ( 0.2500000000000002220, 0.000000000000000000, 0.000000000000000000 ) ) ;
#3425=FACE_OUTER_BOUND ( 'NONE', #10799, .T. ) ;
#3438=DIRECTION ( 'NONE',  ( -1.000000000000000000, -0.000000000000000000, -0.000000000000000000 ) ) ;
#3449=EDGE_CURVE ( 'NONE', #6255, #1188, #7786, .T. ) ;
#3482=VECTOR ( 'NONE', #1783, 1000.000000000000000 ) ;
#3515=ORIENTED_EDGE ( 'NONE', *, *, #3988, .F. ) ;
#3624=VECTOR ( 'NONE', #683, 1000.000000000000000 ) ;
#3628=PLANE ( 'NONE',  #83 ) ;
#3634=ORIENTED_EDGE ( 'NONE', *, *, #13403, .F. ) ;
#3668=CIRCLE ( 'NONE', #11782, 2.041999999999999815 ) ;
#3671=DIRECTION ( 'NONE',  ( -1.000000000000000000, -0.000000000000000000, -0.000000000000000000 ) ) ;
#3742=PLANE ( 'NONE',  #11775 ) ;
#3743=ORIENTED_EDGE ( 'NONE', *, *, #4638, .T. ) ;
#3758=CARTESIAN_POINT ( 'NONE',  ( 5.200000000000002842, 0.000000000000000000, 0.000000000000000000 ) ) ;
#3776=ORIENTED_EDGE ( 'NONE', *, *, #1064, .T. ) ;
#3801=DIRECTION ( 'NONE',  ( 0.000000000000000000, 0.000000000000000000, 1.000000000000000000 ) ) ;
#3813=CYLINDRICAL_SURFACE ( 'NONE', #8603, 2.500000000000000444 ) ;
#3846=LINE ( 'NONE', #13498, #2957 ) ;
#3847=ORIENTED_EDGE ( 'NONE', *, *, #2758, .T. ) ;
#3871=CARTESIAN_POINT ( 'NONE',  ( 0.000000000000000000, 2.357898499370433054, -1.951563910473907981E-15 ) ) ;
#3922=ORIENTED_EDGE ( 'NONE', *, *, #2818, .F. ) ;
#3930=CARTESIAN_POINT ( 'NONE',  ( 2.500000000000000000, 0.000000000000000000, 0.000000000000000000 ) ) ;
#3947=ADVANCED_FACE ( 'NONE', ( #10823, #9736 ), #3140, .T. ) ;
#3949=DIRECTION ( 'NONE',  ( 0.000000000000000000, 0.000000000000000000, 1.000000000000000000 ) ) ;
#3954=VERTEX_POINT ( 'NONE', #8344 ) ;
#3960=PLANE ( 'NONE',  #10247 ) ;
#3973=CIRCLE ( 'NONE', #7213, 2.041999999999999815 ) ;
#3974=EDGE_LOOP ( 'NONE', ( #2989, #5661, #9764, #10731 ) ) ;
#3976=( GEOMETRIC_REPRESENTATION_CONTEXT ( 3 ) GLOBAL_UNCERTAINTY_ASSIGNED_CONTEXT ( ( #5511 ) ) GLOBAL_UNIT_ASSIGNED_CONTEXT ( ( #6883, #10289, #8397 ) ) REPRESENTATION_CONTEXT ( 'NONE', 'WORKASPACE' ) );
#3988=EDGE_CURVE ( 'NONE', #10103, #9376, #3358, .T. ) ;
#4001=ORIENTED_EDGE ( 'NONE', *, *, #9152, .F. ) ;
#4037=DIRECTION ( 'NONE',  ( 1.000000000000000000, 0.000000000000000000, 0.000000000000000000 ) ) ;
#4062=VERTEX_POINT ( 'NONE', #2324 ) ;
#4091=AXIS2_PLACEMENT_3D ( 'NONE', #4770, #13339, #12186 ) ;
#4101=DIRECTION ( 'NONE',  ( 0.000000000000000000, 0.000000000000000000, 1.000000000000000000 ) ) ;
#4109=VECTOR ( 'NONE', #11777, 1000.000000000000000 ) ;
#4118=DIRECTION ( 'NONE',  ( -1.000000000000000000, -0.000000000000000000, -0.000000000000000000 ) ) ;
#4158=CARTESIAN_POINT ( 'NONE',  ( -31.74999999999995737, 0.000000000000000000, 2.500000000000000444 ) ) ;
#4168=ORIENTED_EDGE ( 'NONE', *, *, #7745, .F. ) ;
#4192=DIRECTION ( 'NONE',  ( -1.000000000000000000, -0.000000000000000000, -0.000000000000000000 ) ) ;
#4246=AXIS2_PLACEMENT_3D ( 'NONE', #779, #1890, #1816 ) ;
#4264=CARTESIAN_POINT ( 'NONE',  ( 2.500000000000000000, -1.178949249685213863, 2.042000000000002924 ) ) ;
#4292=DIRECTION ( 'NONE',  ( 0.000000000000000000, 0.000000000000000000, -1.000000000000000000 ) ) ;
#4349=AXIS2_PLACEMENT_3D ( 'NONE', #12047, #8919, #2100 ) ;
#4412=CARTESIAN_POINT ( 'NONE',  ( 0.2500000000000002220, 5.204748896376250699E-16, -4.250000000000000000 ) ) ;
#4420=AXIS2_PLACEMENT_3D ( 'NONE', #5290, #4192, #9630 ) ;
#4424=EDGE_LOOP ( 'NONE', ( #9455, #9629, #11414, #4001, #11661 ) ) ;
#4438=DIRECTION ( 'NONE',  ( 0.000000000000000000, -0.5000000000000012212, -0.8660254037844380415 ) ) ;
#4489=FACE_OUTER_BOUND ( 'NONE', #9216, .T. ) ;
#4550=CIRCLE ( 'NONE', #9417, 2.500000000000000444 ) ;
#4551=DIRECTION ( 'NONE',  ( 0.000000000000000000, -0.4999999999999993894, 0.8660254037844389297 ) ) ;
#4554=EDGE_CURVE ( 'NONE', #1188, #8138, #3341, .T. ) ;
#4556=EDGE_CURVE ( 'NONE', #11681, #247, #10412, .T. ) ;
#4557=ORIENTED_EDGE ( 'NONE', *, *, #5616, .F. ) ;
#4616=APPLICATION_CONTEXT ( 'automotive_design' ) ;
#4626=ADVANCED_FACE ( 'NONE', ( #1340 ), #10175, .F. ) ;
#4638=EDGE_CURVE ( 'NONE', #145, #8138, #2656, .T. ) ;
#4641=DIRECTION ( 'NONE',  ( -1.000000000000000000, -0.000000000000000000, -0.000000000000000000 ) ) ;
#4662=LINE ( 'NONE', #7838, #11260 ) ;
#4663=CARTESIAN_POINT ( 'NONE',  ( 0.2500000000000002220, 0.000000000000000000, 4.000000000000000000 ) ) ;
#4706=VECTOR ( 'NONE', #11868, 1000.000000000000000 ) ;
#4756=CARTESIAN_POINT ( 'NONE',  ( 16.55500000000001393, 0.000000000000000000, 0.000000000000000000 ) ) ;
#4764=DIRECTION ( 'NONE',  ( 0.000000000000000000, 0.000000000000000000, 1.000000000000000000 ) ) ;
#4767=DIRECTION ( 'NONE',  ( -1.000000000000000000, -0.000000000000000000, -0.000000000000000000 ) ) ;
#4770=CARTESIAN_POINT ( 'NONE',  ( 5.200000000000002842, 0.000000000000000000, 0.000000000000000000 ) ) ;
#4780=DIRECTION ( 'NONE',  ( -1.000000000000000000, -0.000000000000000000, -0.000000000000000000 ) ) ;
#4829=AXIS2_PLACEMENT_3D ( 'NONE', #901, #2084, #7380 ) ;
#4840=DIRECTION ( 'NONE',  ( 0.000000000000000000, 0.000000000000000000, 1.000000000000000000 ) ) ;
#4841=DIRECTION ( 'NONE',  ( 0.000000000000000000, -0.4999999999999992784, 0.8660254037844389297 ) ) ;
#4871=VECTOR ( 'NONE', #10054, 1000.000000000000000 ) ;
#4891=EDGE_LOOP ( 'NONE', ( #7491, #9954, #11969, #2704 ) ) ;
#4909=EDGE_CURVE ( 'NONE', #1298, #247, #959, .T. ) ;
#4915=CIRCLE ( 'NONE', #1402, 2.700000000000000622 ) ;
#4939=ORIENTED_EDGE ( 'NONE', *, *, #7636, .F. ) ;
#4950=ORIENTED_EDGE ( 'NONE', *, *, #10400, .F. ) ;
#4964=DIRECTION ( 'NONE',  ( -0.000000000000000000, 0.000000000000000000, 1.000000000000000000 ) ) ;
#5010=ORIENTED_EDGE ( 'NONE', *, *, #13840, .F. ) ;
#5022=VECTOR ( 'NONE', #5581, 1000.000000000000000 ) ;
#5041=CARTESIAN_POINT ( 'NONE',  ( 0.000000000000000000, 0.000000000000000000, 4.000000000000000000 ) ) ;
#5042=AXIS2_PLACEMENT_3D ( 'NONE', #2496, #502, #4964 ) ;
#5076=DIRECTION ( 'NONE',  ( 1.000000000000000000, 0.000000000000000000, 0.000000000000000000 ) ) ;
#5077=DIRECTION ( 'NONE',  ( 1.000000000000000000, 0.000000000000000000, 0.000000000000000000 ) ) ;
#5097=ORIENTED_EDGE ( 'NONE', *, *, #1774, .T. ) ;
#5122=AXIS2_PLACEMENT_3D ( 'NONE', #7374, #4118, #1860 ) ;
#5126=EDGE_CURVE ( 'NONE', #11114, #3954, #8062, .T. ) ;
#5137=CARTESIAN_POINT ( 'NONE',  ( 17.00000000000000000, 2.055000000000000160, 0.000000000000000000 ) ) ;
#5153=DIRECTION ( 'NONE',  ( -0.5000000000000051070, 1.060575238724903217E-16, -0.8660254037844355990 ) ) ;
#5161=VECTOR ( 'NONE', #12929, 1000.000000000000000 ) ;
#5174=DIRECTION ( 'NONE',  ( -1.000000000000000000, -0.000000000000000000, -0.000000000000000000 ) ) ;
#5196=DIRECTION ( 'NONE',  ( 1.000000000000000000, 0.000000000000000000, 0.000000000000000000 ) ) ;
#5199=DIRECTION ( 'NONE',  ( 0.000000000000000000, 0.000000000000000000, 1.000000000000000000 ) ) ;
#5204=CARTESIAN_POINT ( 'NONE',  ( 16.55500000000001393, 0.000000000000000000, 0.000000000000000000 ) ) ;
#5210=CARTESIAN_POINT ( 'NONE',  ( 2.500000000000000000, 1.178949249685218525, 2.041999999999999371 ) ) ;
#5219=DIRECTION ( 'NONE',  ( 0.000000000000000000, 0.000000000000000000, -1.000000000000000000 ) ) ;
#5234=CARTESIAN_POINT ( 'NONE',  ( 0.000000000000000000, 0.000000000000000000, 0.000000000000000000 ) ) ;
#5252=DIRECTION ( 'NONE',  ( -0.000000000000000000, 1.000000000000000000, 1.224646799147353207E-16 ) ) ;
#5266=AXIS2_PLACEMENT_3D ( 'NONE', #14194, #8616, #5219 ) ;
#5272=DIRECTION ( 'NONE',  ( 0.000000000000000000, 0.000000000000000000, -1.000000000000000000 ) ) ;
#5280=CARTESIAN_POINT ( 'NONE',  ( 2.500000000000000000, 1.178949249685213863, -2.042000000000001148 ) ) ;
#5290=CARTESIAN_POINT ( 'NONE',  ( -31.74999999999995737, 0.000000000000000000, 0.000000000000000000 ) ) ;
#5343=EDGE_LOOP ( 'NONE', ( #3847, #1207 ) ) ;
#5354=ADVANCED_FACE ( 'NONE', ( #10703 ), #12942, .T. ) ;
#5423=DIRECTION ( 'NONE',  ( 0.000000000000000000, 0.5000000000000011102, 0.8660254037844380415 ) ) ;
#5431=EDGE_LOOP ( 'NONE', ( #2350, #401, #294, #5666, #13324 ) ) ;
#5445=DIRECTION ( 'NONE',  ( 0.000000000000000000, -0.5000000000000011102, -0.8660254037844379305 ) ) ;
#5474=CARTESIAN_POINT ( 'NONE',  ( 5.200000000000002842, 3.061616997868383634E-16, -2.500000000000000444 ) ) ;
#5478=STYLED_ITEM('',(#14417),#8659);
#5490=ORIENTED_EDGE ( 'NONE', *, *, #7636, .T. ) ;
#5494=AXIS2_PLACEMENT_3D ( 'NONE', #4663, #13556, #8050 ) ;
#5506=CARTESIAN_POINT ( 'NONE',  ( 5.000000000000004441, 5.204748896376250699E-16, -4.250000000000000000 ) ) ;
#5511=UNCERTAINTY_MEASURE_WITH_UNIT (LENGTH_MEASURE( 1.000000000000000082E-05 ), #6883, 'distance_accuracy_value', 'NONE');
#5581=DIRECTION ( 'NONE',  ( 0.000000000000000000, -1.000000000000000000, 1.287488025362403787E-15 ) ) ;
#5590=VECTOR ( 'NONE', #1853, 1000.000000000000000 ) ;
#5604=CARTESIAN_POINT ( 'NONE',  ( 2.500000000000000000, -2.629050547790028551E-15, -2.041999999999999815 ) ) ;
#5606=DIRECTION ( 'NONE',  ( -1.000000000000000000, -0.000000000000000000, -0.000000000000000000 ) ) ;
#5616=EDGE_CURVE ( 'NONE', #11776, #6471, #7913, .T. ) ;
#5629=DIRECTION ( 'NONE',  ( 0.000000000000000000, -0.4999999999999993894, 0.8660254037844389297 ) ) ;
#5644=CARTESIAN_POINT ( 'NONE',  ( 2.500000000000000000, -2.357898499370432610, 3.252606517456513302E-15 ) ) ;
#5647=DIRECTION ( 'NONE',  ( 0.000000000000000000, 1.000000000000000000, -1.471414886128461471E-15 ) ) ;
#5649=ORIENTED_EDGE ( 'NONE', *, *, #3449, .F. ) ;
#5652=CARTESIAN_POINT ( 'NONE',  ( 2.500000000000000000, 0.000000000000000000, 0.000000000000000000 ) ) ;
#5658=ORIENTED_EDGE ( 'NONE', *, *, #8346, .T. ) ;
#5659=EDGE_LOOP ( 'NONE', ( #10005, #4557, #8374, #5490, #10155 ) ) ;
#5661=ORIENTED_EDGE ( 'NONE', *, *, #2818, .T. ) ;
#5666=ORIENTED_EDGE ( 'NONE', *, *, #7593, .T. ) ;
#5720=VECTOR ( 'NONE', #61, 1000.000000000000000 ) ;
#5746=DIRECTION ( 'NONE',  ( -1.000000000000000000, -0.000000000000000000, -0.000000000000000000 ) ) ;
#5754=FACE_BOUND ( 'NONE', #155, .T. ) ;
#5761=DIRECTION ( 'NONE',  ( 0.000000000000000000, 0.000000000000000000, 1.000000000000000000 ) ) ;
#5825=AXIS2_PLACEMENT_3D ( 'NONE', #14175, #814, #11797 ) ;
#5844=FACE_OUTER_BOUND ( 'NONE', #2235, .T. ) ;
#5854=EDGE_LOOP ( 'NONE', ( #13649, #482, #2634, #12848 ) ) ;
#5876=EDGE_CURVE ( 'NONE', #13361, #9311, #11734, .T. ) ;
#5916=DIRECTION ( 'NONE',  ( -1.000000000000000000, -0.000000000000000000, -0.000000000000000000 ) ) ;
#5928=ADVANCED_BREP_SHAPE_REPRESENTATION ( '', ( #8659, #14039 ), #3976 ) ;
#5934=CARTESIAN_POINT ( 'NONE',  ( 17.00000000000000000, 0.000000000000000000, 2.055000000000000160 ) ) ;
#6002=ADVANCED_FACE ( 'NONE', ( #3425 ), #8721, .F. ) ;
#6007=VECTOR ( 'NONE', #12379, 1000.000000000000000 ) ;
#6015=ORIENTED_EDGE ( 'NONE', *, *, #2069, .T. ) ;
#6045=PLANE ( 'NONE',  #5042 ) ;
#6066=FACE_OUTER_BOUND ( 'NONE', #5854, .T. ) ;
#6079=DIRECTION ( 'NONE',  ( -1.000000000000000000, -0.000000000000000000, -0.000000000000000000 ) ) ;
#6104=DIRECTION ( 'NONE',  ( 0.000000000000000000, 0.000000000000000000, -1.000000000000000000 ) ) ;
#6126=ORIENTED_EDGE ( 'NONE', *, *, #11435, .F. ) ;
#6135=LINE ( 'NONE', #522, #13685 ) ;
#6221=LINE ( 'NONE', #10654, #3624 ) ;
#6237=DIRECTION ( 'NONE',  ( 0.000000000000000000, -0.5000000000000012212, -0.8660254037844380415 ) ) ;
#6255=VERTEX_POINT ( 'NONE', #7888 ) ;
#6258=CARTESIAN_POINT ( 'NONE',  ( 0.2500000000000002220, 4.898587196589412829E-16, -4.000000000000000000 ) ) ;
#6270=EDGE_CURVE ( 'NONE', #6471, #568, #12328, .T. ) ;
#6274=DIRECTION ( 'NONE',  ( 0.000000000000000000, -0.8660254037844390407, -0.4999999999999994449 ) ) ;
#6277=LINE ( 'NONE', #5280, #5590 ) ;
#6433=CIRCLE ( 'NONE', #5494, 0.2500000000000002220 ) ;
#6452=EDGE_LOOP ( 'NONE', ( #14041, #1223, #8945 ) ) ;
#6471=VERTEX_POINT ( 'NONE', #13368 ) ;
#6472=DIRECTION ( 'NONE',  ( 0.000000000000000000, -0.5000000000000011102, -0.8660254037844379305 ) ) ;
#6496=CARTESIAN_POINT ( 'NONE',  ( 3.678949249685231848, 0.000000000000000000, 0.000000000000000000 ) ) ;
#6552=DIRECTION ( 'NONE',  ( 0.000000000000000000, 0.000000000000000000, 1.000000000000000000 ) ) ;
#6606=CARTESIAN_POINT ( 'NONE',  ( 2.500000000000000000, 2.357898499370433054, -1.951563910473907981E-15 ) ) ;
#6630=VECTOR ( 'NONE', #14206, 1000.000000000000000 ) ;
#6636=VERTEX_POINT ( 'NONE', #5041 ) ;
#6646=ORIENTED_EDGE ( 'NONE', *, *, #8884, .F. ) ;
#6669=ORIENTED_EDGE ( 'NONE', *, *, #14180, .F. ) ;
#6699=FACE_OUTER_BOUND ( 'NONE', #11664, .T. ) ;
#6734=LINE ( 'NONE', #1208, #440 ) ;
#6765=STYLED_ITEM ( 'NONE', ( #8466 ), #5928 ) ;
#6782=FACE_OUTER_BOUND ( 'NONE', #12692, .T. ) ;
#6784=AXIS2_PLACEMENT_3D ( 'NONE', #10857, #13166, #5272 ) ;
#6785=CIRCLE ( 'NONE', #4246, 4.250000000000000000 ) ;
#6786=DIRECTION ( 'NONE',  ( 0.000000000000000000, 0.4999999999999993339, -0.8660254037844390407 ) ) ;
#6838=ORIENTED_EDGE ( 'NONE', *, *, #9285, .F. ) ;
#6857=EDGE_CURVE ( 'NONE', #13709, #1872, #12639, .T. ) ;
#6867=TOROIDAL_SURFACE ( 'NONE', #9426, 4.000000000000000000, 0.2500000000000000000 ) ;
#6883=( LENGTH_UNIT ( ) NAMED_UNIT ( * ) SI_UNIT ( .MILLI., .METRE. ) );
#6887=CIRCLE ( 'NONE', #4349, 0.2000000000000000944 ) ;
#6894=CARTESIAN_POINT ( 'NONE',  ( 0.000000000000000000, 2.357898499370433054, -1.951563910473907981E-15 ) ) ;
#6896=ORIENTED_EDGE ( 'NONE', *, *, #9416, .F. ) ;
#6902=LINE ( 'NONE', #2478, #5720 ) ;
#6978=CARTESIAN_POINT ( 'NONE',  ( 2.500000000000000000, -1.178949249685213863, 2.042000000000002924 ) ) ;
#7014=EDGE_CURVE ( 'NONE', #6255, #1625, #4662, .T. ) ;
#7048=SHAPE_DEFINITION_REPRESENTATION ( #12247, #10796 ) ;
#7067=ORIENTED_EDGE ( 'NONE', *, *, #13403, .T. ) ;
#7095=CIRCLE ( 'NONE', #4829, 2.500000000000000444 ) ;
#7112=CARTESIAN_POINT ( 'NONE',  ( 2.500000000000000000, 2.357898499370433054, -1.951563910473907981E-15 ) ) ;
#7122=VECTOR ( 'NONE', #5746, 1000.000000000000000 ) ;
#7144=CARTESIAN_POINT ( 'NONE',  ( 2.500000000000000000, -1.178949249685213863, 2.042000000000002924 ) ) ;
#7147=ORIENTED_EDGE ( 'NONE', *, *, #7593, .F. ) ;
#7162=LINE ( 'NONE', #12750, #10679 ) ;
#7202=DIRECTION ( 'NONE',  ( 0.000000000000000000, 1.000000000000000000, -1.471414886128461471E-15 ) ) ;
#7213=AXIS2_PLACEMENT_3D ( 'NONE', #9101, #9319, #3801 ) ;
#7226=LINE ( 'NONE', #5210, #2782 ) ;
#7232=EDGE_CURVE ( 'NONE', #2861, #6636, #3175, .T. ) ;
#7238=DIRECTION ( 'NONE',  ( 0.000000000000000000, 0.000000000000000000, 1.000000000000000000 ) ) ;
#7252=CARTESIAN_POINT ( 'NONE',  ( 0.000000000000000000, 2.357898499370433054, -1.951563910473907981E-15 ) ) ;
#7284=EDGE_CURVE ( 'NONE', #11114, #13361, #1811, .T. ) ;
#7327=PLANE ( 'NONE',  #7406 ) ;
#7356=CIRCLE ( 'NONE', #10610, 4.250000000000000000 ) ;
#7359=EDGE_CURVE ( 'NONE', #13709, #13005, #9053, .T. ) ;
#7365=DIRECTION ( 'NONE',  ( 0.000000000000000000, 0.000000000000000000, -1.000000000000000000 ) ) ;
#7374=CARTESIAN_POINT ( 'NONE',  ( 2.500000000000000000, 0.000000000000000000, 0.000000000000000000 ) ) ;
#7375=AXIS2_PLACEMENT_3D ( 'NONE', #4756, #7930, #5761 ) ;
#7380=DIRECTION ( 'NONE',  ( 0.000000000000000000, 0.000000000000000000, -1.000000000000000000 ) ) ;
#7385=SURFACE_STYLE_USAGE ( .BOTH. , #8618 ) ;
#7406=AXIS2_PLACEMENT_3D ( 'NONE', #7478, #9517, #6104 ) ;
#7407=FACE_OUTER_BOUND ( 'NONE', #2168, .T. ) ;
#7414=EDGE_LOOP ( 'NONE', ( #12765, #10276, #8170, #9381 ) ) ;
#7454=LINE ( 'NONE', #14192, #12657 ) ;
#7475=DIRECTION ( 'NONE',  ( 0.000000000000000000, 0.000000000000000000, 1.000000000000000000 ) ) ;
#7478=CARTESIAN_POINT ( 'NONE',  ( 2.500000000000000000, 2.357898499370433054, -1.951563910473907981E-15 ) ) ;
#7491=ORIENTED_EDGE ( 'NONE', *, *, #7284, .F. ) ;
#7495=DIRECTION ( 'NONE',  ( 0.000000000000000000, 0.000000000000000000, 1.000000000000000000 ) ) ;
#7575=LINE ( 'NONE', #12014, #4706 ) ;
#7578=APPLICATION_CONTEXT ( 'automotive_design' ) ;
#7593=EDGE_CURVE ( 'NONE', #1872, #12690, #11280, .T. ) ;
#7609=FACE_OUTER_BOUND ( 'NONE', #7414, .T. ) ;
#7619=ORIENTED_EDGE ( 'NONE', *, *, #4556, .T. ) ;
#7636=EDGE_CURVE ( 'NONE', #12690, #794, #7454, .T. ) ;
#7652=CARTESIAN_POINT ( 'NONE',  ( 2.500000000000000000, 1.178949249685213863, -2.042000000000001148 ) ) ;
#7674=( GEOMETRIC_REPRESENTATION_CONTEXT ( 3 ) GLOBAL_UNCERTAINTY_ASSIGNED_CONTEXT ( ( #1588 ) ) GLOBAL_UNIT_ASSIGNED_CONTEXT ( ( #2896, #1941, #9573 ) ) REPRESENTATION_CONTEXT ( 'NONE', 'WORKASPACE' ) );
#7682=CARTESIAN_POINT ( 'NONE',  ( 17.00000000000000000, 0.000000000000000000, 2.055000000000000160 ) ) ;
#7710=ORIENTED_EDGE ( 'NONE', *, *, #7014, .F. ) ;
#7723=CARTESIAN_POINT ( 'NONE',  ( -31.74999999999995737, 0.000000000000000000, 4.250000000000000000 ) ) ;
#7732=ADVANCED_FACE ( 'NONE', ( #8684 ), #12029, .F. ) ;
#7745=EDGE_CURVE ( 'NONE', #3306, #11114, #6221, .T. ) ;
#7748=CARTESIAN_POINT ( 'NONE',  ( 2.500000000000000000, 1.178949249685213863, -2.042000000000001148 ) ) ;
#7786=LINE ( 'NONE', #2288, #10690 ) ;
#7787=VECTOR ( 'NONE', #7202, 1000.000000000000000 ) ;
#7838=CARTESIAN_POINT ( 'NONE',  ( 2.500000000000000000, 2.357898499370433054, -1.951563910473907981E-15 ) ) ;
#7855=AXIS2_PLACEMENT_3D ( 'NONE', #8010, #4767, #1481 ) ;
#7864=FACE_OUTER_BOUND ( 'NONE', #2097, .T. ) ;
#7870=CARTESIAN_POINT ( 'NONE',  ( 0.2500000000000002220, 0.000000000000000000, 0.000000000000000000 ) ) ;
#7876=ORIENTED_EDGE ( 'NONE', *, *, #7232, .F. ) ;
#7888=CARTESIAN_POINT ( 'NONE',  ( 2.500000000000000000, 2.357898499370433054, -1.951563910473907981E-15 ) ) ;
#7913=LINE ( 'NONE', #6978, #7122 ) ;
#7916=EDGE_CURVE ( 'NONE', #247, #11681, #11053, .T. ) ;
#7930=DIRECTION ( 'NONE',  ( -1.000000000000000000, -0.000000000000000000, -0.000000000000000000 ) ) ;
#7959=ORIENTED_EDGE ( 'NONE', *, *, #1342, .F. ) ;
#7962=DIRECTION ( 'NONE',  ( 1.000000000000000000, 0.000000000000000000, 0.000000000000000000 ) ) ;
#7991=EDGE_CURVE ( 'NONE', #11776, #145, #13732, .T. ) ;
#7998=ORIENTED_EDGE ( 'NONE', *, *, #12376, .F. ) ;
#8010=CARTESIAN_POINT ( 'NONE',  ( 2.500000000000000000, 0.000000000000000000, 0.000000000000000000 ) ) ;
#8017=VERTEX_POINT ( 'NONE', #428 ) ;
#8047=EDGE_LOOP ( 'NONE', ( #8499, #395, #1319, #8261, #3776 ) ) ;
#8050=DIRECTION ( 'NONE',  ( 0.000000000000000000, 0.000000000000000000, -1.000000000000000000 ) ) ;
#8062=CIRCLE ( 'NONE', #7375, 2.500000000000000444 ) ;
#8138=VERTEX_POINT ( 'NONE', #1088 ) ;
#8170=ORIENTED_EDGE ( 'NONE', *, *, #11962, .F. ) ;
#8184=VERTEX_POINT ( 'NONE', #2554 ) ;
#8192=LINE ( 'NONE', #7112, #1778 ) ;
#8194=CARTESIAN_POINT ( 'NONE',  ( 2.500000000000000000, -2.357898499370432610, 3.252606517456513302E-15 ) ) ;
#8201=ORIENTED_EDGE ( 'NONE', *, *, #13625, .F. ) ;
#8206=DIRECTION ( 'NONE',  ( 0.000000000000000000, 0.000000000000000000, 1.000000000000000000 ) ) ;
#8261=ORIENTED_EDGE ( 'NONE', *, *, #2878, .T. ) ;
#8262=EDGE_CURVE ( 'NONE', #9712, #3306, #14055, .T. ) ;
#8270=PRODUCT_DEFINITION_CONTEXT ( 'detailed design', #7578, 'design' ) ;
#8296=EDGE_CURVE ( 'NONE', #9376, #278, #6902, .T. ) ;
#8314=CARTESIAN_POINT ( 'NONE',  ( -31.74999999999995737, 5.204748896376250699E-16, -4.250000000000000000 ) ) ;
#8337=ORIENTED_EDGE ( 'NONE', *, *, #7991, .F. ) ;
#8343=DIRECTION ( 'NONE',  ( 0.000000000000000000, 0.000000000000000000, 1.000000000000000000 ) ) ;
#8344=CARTESIAN_POINT ( 'NONE',  ( 16.55500000000001393, 0.000000000000000000, 2.500000000000000444 ) ) ;
#8346=EDGE_CURVE ( 'NONE', #794, #1872, #12841, .T. ) ;
#8356=CARTESIAN_POINT ( 'NONE',  ( 0.000000000000000000, -2.357898499370432610, 3.252606517456513302E-15 ) ) ;
#8374=ORIENTED_EDGE ( 'NONE', *, *, #1428, .T. ) ;
#8386=DIRECTION ( 'NONE',  ( -1.000000000000000000, -0.000000000000000000, -0.000000000000000000 ) ) ;
#8397=( NAMED_UNIT ( * ) SI_UNIT ( $, .STERADIAN. ) SOLID_ANGLE_UNIT ( ) );
#8414=DIRECTION ( 'NONE',  ( 0.000000000000000000, 0.000000000000000000, -1.000000000000000000 ) ) ;
#8430=DIRECTION ( 'NONE',  ( -1.000000000000000000, -0.000000000000000000, -0.000000000000000000 ) ) ;
#8439=ADVANCED_FACE ( 'NONE', ( #7609 ), #1548, .T. ) ;
#8466=PRESENTATION_STYLE_ASSIGNMENT (( #7385 ) ) ;
#8484=DIRECTION ( 'NONE',  ( -1.000000000000000000, -0.000000000000000000, -0.000000000000000000 ) ) ;
#8499=ORIENTED_EDGE ( 'NONE', *, *, #3300, .F. ) ;
#8538=FACE_OUTER_BOUND ( 'NONE', #4891, .T. ) ;
#8590=EDGE_CURVE ( 'NONE', #12690, #145, #3207, .T. ) ;
#8603=AXIS2_PLACEMENT_3D ( 'NONE', #13522, #5916, #4764 ) ;
#8609=DIRECTION ( 'NONE',  ( 0.000000000000000000, 0.8660254037844380415, -0.5000000000000011102 ) ) ;
#8611=TOROIDAL_SURFACE ( 'NONE', #10467, 2.700000000000000622, 0.2000000000000000111 ) ;
#8616=DIRECTION ( 'NONE',  ( 1.000000000000000000, 0.000000000000000000, 0.000000000000000000 ) ) ;
#8618=SURFACE_SIDE_STYLE ('',( #1719 ) ) ;
#8659=MANIFOLD_SOLID_BREP ( 'Hex', #12157 ) ;
#8684=FACE_OUTER_BOUND ( 'NONE', #9615, .T. ) ;
#8687=PLANE ( 'NONE',  #5266 ) ;
#8713=ORIENTED_EDGE ( 'NONE', *, *, #14180, .T. ) ;
#8721=TOROIDAL_SURFACE ( 'NONE', #4091, 2.700000000000000622, 0.2000000000000000111 ) ;
#8746=CARTESIAN_POINT ( 'NONE',  ( 2.500000000000000000, -2.357898499370432610, 3.252606517456513302E-15 ) ) ;
#8808=ADVANCED_FACE ( 'NONE', ( #9849 ), #8687, .F. ) ;
#8840=AXIS2_PLACEMENT_3D ( 'NONE', #5137, #4037, #7365 ) ;
#8884=EDGE_CURVE ( 'NONE', #8184, #13361, #7095, .T. ) ;
#8889=DIRECTION ( 'NONE',  ( 0.000000000000000000, 0.000000000000000000, -1.000000000000000000 ) ) ;
#8919=DIRECTION ( 'NONE',  ( 0.000000000000000000, 1.000000000000000000, -1.224646799147353207E-16 ) ) ;
#8945=ORIENTED_EDGE ( 'NONE', *, *, #1064, .F. ) ;
#8955=FACE_OUTER_BOUND ( 'NONE', #5431, .T. ) ;
#8972=ADVANCED_FACE ( 'NONE', ( #4489 ), #6867, .T. ) ;
#8980=FACE_OUTER_BOUND ( 'NONE', #13118, .T. ) ;
#9009=CARTESIAN_POINT ( 'NONE',  ( 17.00000000000000000, 0.000000000000000000, 0.000000000000000000 ) ) ;
#9053=LINE ( 'NONE', #7748, #5022 ) ;
#9056=DIRECTION ( 'NONE',  ( 0.000000000000000000, 0.000000000000000000, 1.000000000000000000 ) ) ;
#9067=CARTESIAN_POINT ( 'NONE',  ( 2.500000000000000000, 2.357898499370433054, -1.951563910473907981E-15 ) ) ;
#9095=FACE_OUTER_BOUND ( 'NONE', #1484, .T. ) ;
#9100=AXIS2_PLACEMENT_3D ( 'NONE', #13960, #2943, #1763 ) ;
#9101=CARTESIAN_POINT ( 'NONE',  ( 2.500000000000000000, 0.000000000000000000, 0.000000000000000000 ) ) ;
#9116=EDGE_CURVE ( 'NONE', #13005, #2622, #6135, .T. ) ;
#9122=ADVANCED_FACE ( 'NONE', ( #6066 ), #3813, .T. ) ;
#9135=FACE_OUTER_BOUND ( 'NONE', #12146, .T. ) ;
#9143=ORIENTED_EDGE ( 'NONE', *, *, #4909, .F. ) ;
#9152=EDGE_CURVE ( 'NONE', #9376, #13709, #6277, .T. ) ;
#9156=ADVANCED_FACE ( 'NONE', ( #9769 ), #2953, .F. ) ;
#9174=CYLINDRICAL_SURFACE ( 'NONE', #12803, 4.250000000000000000 ) ;
#9189=LINE ( 'NONE', #8314, #3482 ) ;
#9199=AXIS2_PLACEMENT_3D ( 'NONE', #1617, #9391, #5199 ) ;
#9216=EDGE_LOOP ( 'NONE', ( #13646, #11603, #12314, #5010 ) ) ;
#9220=VECTOR ( 'NONE', #11635, 1000.000000000000114 ) ;
#9258=ADVANCED_FACE ( 'NONE', ( #10863 ), #673, .T. ) ;
#9285=EDGE_CURVE ( 'NONE', #1872, #13005, #2146, .T. ) ;
#9311=VERTEX_POINT ( 'NONE', #9983 ) ;
#9319=DIRECTION ( 'NONE',  ( -1.000000000000000000, -0.000000000000000000, -0.000000000000000000 ) ) ;
#9359=ORIENTED_EDGE ( 'NONE', *, *, #6857, .F. ) ;
#9376=VERTEX_POINT ( 'NONE', #7652 ) ;
#9379=ORIENTED_EDGE ( 'NONE', *, *, #1342, .T. ) ;
#9381=ORIENTED_EDGE ( 'NONE', *, *, #9969, .F. ) ;
#9389=AXIS2_PLACEMENT_3D ( 'NONE', #10988, #11057, #13292 ) ;
#9391=DIRECTION ( 'NONE',  ( -1.000000000000000000, -0.000000000000000000, -0.000000000000000000 ) ) ;
#9398=FACE_OUTER_BOUND ( 'NONE', #10957, .T. ) ;
#9416=EDGE_CURVE ( 'NONE', #145, #1188, #3973, .T. ) ;
#9417=AXIS2_PLACEMENT_3D ( 'NONE', #5204, #14025, #4101 ) ;
#9418=DIRECTION ( 'NONE',  ( 0.000000000000000000, 0.000000000000000000, 1.000000000000000000 ) ) ;
#9421=DIRECTION ( 'NONE',  ( -0.7071067811865369146, 0.000000000000000000, 0.7071067811865582309 ) ) ;
#9426=AXIS2_PLACEMENT_3D ( 'NONE', #3398, #13456, #11155 ) ;
#9441=CARTESIAN_POINT ( 'NONE',  ( 5.000000000000004441, 0.000000000000000000, 0.000000000000000000 ) ) ;
#9455=ORIENTED_EDGE ( 'NONE', *, *, #10401, .T. ) ;
#9487=DIRECTION ( 'NONE',  ( 0.000000000000000000, 0.000000000000000000, -1.000000000000000000 ) ) ;
#9496=CONICAL_SURFACE ( 'NONE', #1612, 2.055000000000000160, 0.7853981633974633780 ) ;
#9515=DIRECTION ( 'NONE',  ( 0.000000000000000000, 0.4999999999999993339, -0.8660254037844390407 ) ) ;
#9517=DIRECTION ( 'NONE',  ( 1.000000000000000000, 0.000000000000000000, 0.000000000000000000 ) ) ;
#9573=( NAMED_UNIT ( * ) SI_UNIT ( $, .STERADIAN. ) SOLID_ANGLE_UNIT ( ) );
#9590=CARTESIAN_POINT ( 'NONE',  ( 5.000000000000000888, 0.000000000000000000, 0.000000000000000000 ) ) ;
#9615=EDGE_LOOP ( 'NONE', ( #9642, #13576, #2311 ) ) ;
#9619=DIRECTION ( 'NONE',  ( 0.000000000000000000, 0.4999999999999993894, -0.8660254037844389297 ) ) ;
#9629=ORIENTED_EDGE ( 'NONE', *, *, #9116, .F. ) ;
#9630=DIRECTION ( 'NONE',  ( 0.000000000000000000, 0.000000000000000000, 1.000000000000000000 ) ) ;
#9641=FILL_AREA_STYLE ('',( #11671 ) ) ;
#9642=ORIENTED_EDGE ( 'NONE', *, *, #1428, .F. ) ;
#9654=DIRECTION ( 'NONE',  ( -1.000000000000000000, -0.000000000000000000, -0.000000000000000000 ) ) ;
#9660=CARTESIAN_POINT ( 'NONE',  ( 0.000000000000000000, 5.051668046482832750E-16, -4.000000000000000000 ) ) ;
#9661=AXIS2_PLACEMENT_3D ( 'NONE', #1640, #6079, #7238 ) ;
#9712=VERTEX_POINT ( 'NONE', #7682 ) ;
#9728=ORIENTED_EDGE ( 'NONE', *, *, #8296, .F. ) ;
#9730=CARTESIAN_POINT ( 'NONE',  ( 0.000000000000000000, 0.000000000000000000, 0.000000000000000000 ) ) ;
#9736=FACE_OUTER_BOUND ( 'NONE', #11861, .T. ) ;
#9746=AXIS2_PLACEMENT_3D ( 'NONE', #2032, #10531, #1738 ) ;
#9764=ORIENTED_EDGE ( 'NONE', *, *, #4909, .T. ) ;
#9769=FACE_OUTER_BOUND ( 'NONE', #4424, .T. ) ;
#9801=CARTESIAN_POINT ( 'NONE',  ( -31.74999999999995737, 3.061616997868383634E-16, -2.500000000000000444 ) ) ;
#9849=FACE_OUTER_BOUND ( 'NONE', #6452, .T. ) ;
#9878=AXIS2_PLACEMENT_3D ( 'NONE', #5234, #9654, #7475 ) ;
#9954=ORIENTED_EDGE ( 'NONE', *, *, #5126, .T. ) ;
#9969=EDGE_CURVE ( 'NONE', #9712, #3954, #12543, .T. ) ;
#9983=CARTESIAN_POINT ( 'NONE',  ( 5.000000000000002665, 0.000000000000000000, -2.700000000000000622 ) ) ;
#10005=ORIENTED_EDGE ( 'NONE', *, *, #6270, .F. ) ;
#10054=DIRECTION ( 'NONE',  ( -1.000000000000000000, -0.000000000000000000, -0.000000000000000000 ) ) ;
#10059=CARTESIAN_POINT ( 'NONE',  ( 2.500000000000000000, 1.768423874527822681, -1.021000000000002794 ) ) ;
#10070=ORIENTED_EDGE ( 'NONE', *, *, #9969, .T. ) ;
#10103=VERTEX_POINT ( 'NONE', #10059 ) ;
#10144=ORIENTED_EDGE ( 'NONE', *, *, #9285, .T. ) ;
#10155=ORIENTED_EDGE ( 'NONE', *, *, #14276, .T. ) ;
#10166=DIRECTION ( 'NONE',  ( 0.000000000000000000, -0.5000000000000012212, -0.8660254037844380415 ) ) ;
#10168=ADVANCED_FACE ( 'NONE', ( #7864 ), #9174, .T. ) ;
#10175=CONICAL_SURFACE ( 'NONE', #7855, 2.041999999999999815, 1.047197551196591858 ) ;
#10180=CARTESIAN_POINT ( 'NONE',  ( -31.74999999999995737, 0.000000000000000000, 0.000000000000000000 ) ) ;
#10183=PLANE ( 'NONE',  #12695 ) ;
#10187=AXIS2_PLACEMENT_3D ( 'NONE', #9590, #5174, #8414 ) ;
#10193=ADVANCED_FACE ( 'NONE', ( #9398 ), #3960, .T. ) ;
#10199=AXIS2_PLACEMENT_3D ( 'NONE', #2428, #11278, #12298 ) ;
#10247=AXIS2_PLACEMENT_3D ( 'NONE', #518, #6274, #9619 ) ;
#10265=ORIENTED_EDGE ( 'NONE', *, *, #13840, .T. ) ;
#10276=ORIENTED_EDGE ( 'NONE', *, *, #7745, .T. ) ;
#10289=( NAMED_UNIT ( * ) PLANE_ANGLE_UNIT ( ) SI_UNIT ( $, .RADIAN. ) );
#10318=DIRECTION ( 'NONE',  ( -1.000000000000000000, -0.000000000000000000, -0.000000000000000000 ) ) ;
#10334=CARTESIAN_POINT ( 'NONE',  ( -31.74999999999995737, 0.000000000000000000, 0.000000000000000000 ) ) ;
#10369=DIRECTION ( 'NONE',  ( 1.000000000000000000, 0.000000000000000000, 0.000000000000000000 ) ) ;
#10400=EDGE_CURVE ( 'NONE', #13361, #8184, #264, .T. ) ;
#10401=EDGE_CURVE ( 'NONE', #278, #2622, #7575, .T. ) ;
#10412=CIRCLE ( 'NONE', #3014, 4.250000000000000000 ) ;
#10465=CARTESIAN_POINT ( 'NONE',  ( 5.000000000000004441, 0.000000000000000000, 4.250000000000000000 ) ) ;
#10467=AXIS2_PLACEMENT_3D ( 'NONE', #3758, #1561, #535 ) ;
#10504=ADVANCED_FACE ( 'NONE', ( #11713 ), #2798, .F. ) ;
#10508=CARTESIAN_POINT ( 'NONE',  ( 0.000000000000000000, 0.000000000000000000, 0.000000000000000000 ) ) ;
#10531=DIRECTION ( 'NONE',  ( 1.000000000000000000, 0.000000000000000000, 0.000000000000000000 ) ) ;
#10576=AXIS2_PLACEMENT_3D ( 'NONE', #2933, #5196, #3949 ) ;
#10580=( NAMED_UNIT ( * ) PLANE_ANGLE_UNIT ( ) SI_UNIT ( $, .RADIAN. ) );
#10593=CIRCLE ( 'NONE', #128, 0.2500000000000002220 ) ;
#10604=AXIS2_PLACEMENT_3D ( 'NONE', #9009, #5606, #11257 ) ;
#10610=AXIS2_PLACEMENT_3D ( 'NONE', #9441, #11684, #850 ) ;
#10654=CARTESIAN_POINT ( 'NONE',  ( 17.00000000000000000, 2.516649172247811061E-16, -2.055000000000000160 ) ) ;
#10679=VECTOR ( 'NONE', #5153, 1000.000000000000114 ) ;
#10690=VECTOR ( 'NONE', #5629, 1000.000000000000114 ) ;
#10703=FACE_OUTER_BOUND ( 'NONE', #2184, .T. ) ;
#10731=ORIENTED_EDGE ( 'NONE', *, *, #7916, .T. ) ;
#10768=DIRECTION ( 'NONE',  ( -1.000000000000000000, -0.000000000000000000, -0.000000000000000000 ) ) ;
#10796=SHAPE_REPRESENTATION ( 'socket head cap screw_iso_ISO 4762 M5 x 12 - 12N', ( #14039 ), #3976 ) ;
#10799=EDGE_LOOP ( 'NONE', ( #6669, #4950, #973, #6126 ) ) ;
#10823=FACE_BOUND ( 'NONE', #5343, .T. ) ;
#10857=CARTESIAN_POINT ( 'NONE',  ( 5.200000000000002842, 0.000000000000000000, 0.000000000000000000 ) ) ;
#10863=FACE_OUTER_BOUND ( 'NONE', #11182, .T. ) ;
#10893=CIRCLE ( 'NONE', #10187, 2.700000000000000622 ) ;
#10957=EDGE_LOOP ( 'NONE', ( #3634, #7710, #1841, #272, #6015 ) ) ;
#10988=CARTESIAN_POINT ( 'NONE',  ( 2.500000000000000000, 2.357898499370433054, -1.951563910473907981E-15 ) ) ;
#10994=ORIENTED_EDGE ( 'NONE', *, *, #2878, .F. ) ;
#11013=DIRECTION ( 'NONE',  ( 0.000000000000000000, 0.000000000000000000, 1.000000000000000000 ) ) ;
#11042=ORIENTED_EDGE ( 'NONE', *, *, #11218, .T. ) ;
#11053=CIRCLE ( 'NONE', #10576, 4.250000000000000000 ) ;
#11057=DIRECTION ( 'NONE',  ( 0.000000000000000000, 0.8660254037844380415, -0.5000000000000012212 ) ) ;
#11114=VERTEX_POINT ( 'NONE', #3201 ) ;
#11155=DIRECTION ( 'NONE',  ( 0.000000000000000000, 0.000000000000000000, 1.000000000000000000 ) ) ;
#11182=EDGE_LOOP ( 'NONE', ( #1523, #8201 ) ) ;
#11218=EDGE_CURVE ( 'NONE', #6471, #8017, #6734, .T. ) ;
#11237=LINE ( 'NONE', #387, #1787 ) ;
#11257=DIRECTION ( 'NONE',  ( 0.000000000000000000, 0.000000000000000000, 1.000000000000000000 ) ) ;
#11260=VECTOR ( 'NONE', #3438, 1000.000000000000000 ) ;
#11270=AXIS2_PLACEMENT_3D ( 'NONE', #9730, #12838, #3130 ) ;
#11276=ADVANCED_FACE ( 'NONE', ( #307 ), #8611, .F. ) ;
#11278=DIRECTION ( 'NONE',  ( -1.000000000000000000, -0.000000000000000000, -0.000000000000000000 ) ) ;
#11280=CIRCLE ( 'NONE', #9661, 2.041999999999999815 ) ;
#11359=CIRCLE ( 'NONE', #5122, 2.041999999999999815 ) ;
#11367=CARTESIAN_POINT ( 'NONE',  ( 2.500000000000000000, -1.178949249685213863, 2.042000000000002924 ) ) ;
#11401=DIRECTION ( 'NONE',  ( -0.5000000000000051070, 0.000000000000000000, 0.8660254037844355990 ) ) ;
#11414=ORIENTED_EDGE ( 'NONE', *, *, #7359, .F. ) ;
#11418=VECTOR ( 'NONE', #6237, 999.9999999999998863 ) ;
#11419=ORIENTED_EDGE ( 'NONE', *, *, #2758, .F. ) ;
#11435=EDGE_CURVE ( 'NONE', #4062, #9311, #4915, .T. ) ;
#11512=CARTESIAN_POINT ( 'NONE',  ( 17.00000000000000000, 0.000000000000000000, 0.000000000000000000 ) ) ;
#11592=AXIS2_PLACEMENT_3D ( 'NONE', #4264, #8609, #5423 ) ;
#11603=ORIENTED_EDGE ( 'NONE', *, *, #12376, .T. ) ;
#11635=DIRECTION ( 'NONE',  ( 0.000000000000000000, -0.4999999999999993894, 0.8660254037844389297 ) ) ;
#11661=ORIENTED_EDGE ( 'NONE', *, *, #8296, .T. ) ;
#11664=EDGE_LOOP ( 'NONE', ( #5097, #9728, #3515, #707, #13070 ) ) ;
#11671=FILL_AREA_STYLE_COLOUR ( '', #3302 ) ;
#11681=VERTEX_POINT ( 'NONE', #4412 ) ;
#11684=DIRECTION ( 'NONE',  ( -1.000000000000000000, -0.000000000000000000, -0.000000000000000000 ) ) ;
#11700=LINE ( 'NONE', #4158, #4109 ) ;
#11705=CARTESIAN_POINT ( 'NONE',  ( 17.00000000000000000, 0.000000000000000000, 0.000000000000000000 ) ) ;
#11713=FACE_OUTER_BOUND ( 'NONE', #14272, .T. ) ;
#11727=DIRECTION ( 'NONE',  ( -1.000000000000000000, -0.000000000000000000, -0.000000000000000000 ) ) ;
#11734=CIRCLE ( 'NONE', #1283, 0.2000000000000000944 ) ;
#11743=SHAPE_REPRESENTATION_RELATIONSHIP ( 'NONE' , 'NONE' ,  #10796, #5928 ) ;
#11746=VECTOR ( 'NONE', #9515, 1000.000000000000000 ) ;
#11775=AXIS2_PLACEMENT_3D ( 'NONE', #2732, #297, #4841 ) ;
#11776=VERTEX_POINT ( 'NONE', #7144 ) ;
#11777=DIRECTION ( 'NONE',  ( -1.000000000000000000, -0.000000000000000000, -0.000000000000000000 ) ) ;
#11782=AXIS2_PLACEMENT_3D ( 'NONE', #3930, #561, #8343 ) ;
#11797=DIRECTION ( 'NONE',  ( 0.000000000000000000, 1.000000000000000000, -1.287488025362403787E-15 ) ) ;
#11824=CARTESIAN_POINT ( 'NONE',  ( 2.500000000000000000, -1.768423874527823791, -1.020999999999998353 ) ) ;
#11857=VECTOR ( 'NONE', #6786, 1000.000000000000000 ) ;
#11861=EDGE_LOOP ( 'NONE', ( #12059, #3922 ) ) ;
#11868=DIRECTION ( 'NONE',  ( 0.000000000000000000, -1.000000000000000000, 1.287488025362403787E-15 ) ) ;
#11901=ORIENTED_EDGE ( 'NONE', *, *, #11218, .F. ) ;
#11909=CARTESIAN_POINT ( 'NONE',  ( 17.00000000000000000, 0.000000000000000000, 0.000000000000000000 ) ) ;
#11962=EDGE_CURVE ( 'NONE', #3954, #11114, #4550, .T. ) ;
#11969=ORIENTED_EDGE ( 'NONE', *, *, #12339, .T. ) ;
#12014=CARTESIAN_POINT ( 'NONE',  ( 0.000000000000000000, 1.178949249685213863, -2.042000000000001148 ) ) ;
#12026=CARTESIAN_POINT ( 'NONE',  ( 5.000000000000000888, 0.000000000000000000, 0.000000000000000000 ) ) ;
#12029=PLANE ( 'NONE',  #125 ) ;
#12047=CARTESIAN_POINT ( 'NONE',  ( 5.200000000000002842, 3.306546357697854226E-16, 2.700000000000000622 ) ) ;
#12059=ORIENTED_EDGE ( 'NONE', *, *, #14032, .F. ) ;
#12068=CARTESIAN_POINT ( 'NONE',  ( 2.500000000000000000, 0.000000000000000000, 0.000000000000000000 ) ) ;
#12106=PRODUCT_DEFINITION_FORMATION_WITH_SPECIFIED_SOURCE ( 'ANY', '', #2407, .NOT_KNOWN. ) ;
#12146=EDGE_LOOP ( 'NONE', ( #3743, #13703, #6896 ) ) ;
#12157=CLOSED_SHELL ( 'NONE', ( #3393, #8972, #11276, #10168, #9122, #8439, #12320, #9258, #853, #1055, #3947, #12250, #6002, #5354, #10193, #10504, #1078, #13140, #9156, #2467, #13323, #506, #7732, #273, #2745, #8808, #4626 ) ) ;
#12186=DIRECTION ( 'NONE',  ( 0.000000000000000000, 0.000000000000000000, -1.000000000000000000 ) ) ;
#12247=PRODUCT_DEFINITION_SHAPE ( 'NONE', 'NONE',  #1599 ) ;
#12250=ADVANCED_FACE ( 'NONE', ( #2639 ), #216, .T. ) ;
#12298=DIRECTION ( 'NONE',  ( 0.000000000000000000, 0.000000000000000000, 1.000000000000000000 ) ) ;
#12314=ORIENTED_EDGE ( 'NONE', *, *, #14111, .F. ) ;
#12320=ADVANCED_FACE ( 'NONE', ( #5754, #9095 ), #6045, .T. ) ;
#12328=LINE ( 'NONE', #2393, #2459 ) ;
#12335=CARTESIAN_POINT ( 'NONE',  ( 0.000000000000000000, 1.178949249685213863, -2.042000000000001148 ) ) ;
#12339=EDGE_CURVE ( 'NONE', #3954, #8184, #11700, .T. ) ;
#12376=EDGE_CURVE ( 'NONE', #11681, #2861, #10593, .T. ) ;
#12379=DIRECTION ( 'NONE',  ( 0.000000000000000000, 1.000000000000000000, -1.471414886128461471E-15 ) ) ;
#12406=ORIENTED_EDGE ( 'NONE', *, *, #5126, .F. ) ;
#12457=AXIS2_PLACEMENT_3D ( 'NONE', #11909, #8484, #3137 ) ;
#12477=ORIENTED_EDGE ( 'NONE', *, *, #8346, .F. ) ;
#12481=ORIENTED_EDGE ( 'NONE', *, *, #7232, .T. ) ;
#12543=LINE ( 'NONE', #5934, #3319 ) ;
#12603=( LENGTH_UNIT ( ) NAMED_UNIT ( * ) SI_UNIT ( .MILLI., .METRE. ) );
#12629=AXIS2_PLACEMENT_3D ( 'NONE', #12758, #10369, #2830 ) ;
#12639=CIRCLE ( 'NONE', #565, 2.041999999999999815 ) ;
#12657=VECTOR ( 'NONE', #3041, 1000.000000000000114 ) ;
#12686=FACE_OUTER_BOUND ( 'NONE', #12924, .T. ) ;
#12690=VERTEX_POINT ( 'NONE', #329 ) ;
#12692=EDGE_LOOP ( 'NONE', ( #1289, #6838, #9359 ) ) ;
#12695=AXIS2_PLACEMENT_3D ( 'NONE', #1026, #2143, #8889 ) ;
#12718=UNCERTAINTY_MEASURE_WITH_UNIT (LENGTH_MEASURE( 1.000000000000000082E-05 ), #12603, 'distance_accuracy_value', 'NONE');
#12750=CARTESIAN_POINT ( 'NONE',  ( 2.500000000000000000, 2.500728763858895382E-16, -2.041999999999999815 ) ) ;
#12758=CARTESIAN_POINT ( 'NONE',  ( 2.500000000000000000, 2.357898499370433054, -1.951563910473907981E-15 ) ) ;
#12765=ORIENTED_EDGE ( 'NONE', *, *, #8262, .T. ) ;
#12803=AXIS2_PLACEMENT_3D ( 'NONE', #10334, #3671, #4840 ) ;
#12838=DIRECTION ( 'NONE',  ( -1.000000000000000000, -0.000000000000000000, -0.000000000000000000 ) ) ;
#12841=LINE ( 'NONE', #8194, #11746 ) ;
#12848=ORIENTED_EDGE ( 'NONE', *, *, #12339, .F. ) ;
#12875=ORIENTED_EDGE ( 'NONE', *, *, #896, .T. ) ;
#12889=( GEOMETRIC_REPRESENTATION_CONTEXT ( 3 ) GLOBAL_UNCERTAINTY_ASSIGNED_CONTEXT ( ( #12718 ) ) GLOBAL_UNIT_ASSIGNED_CONTEXT ( ( #12603, #10580, #313 ) ) REPRESENTATION_CONTEXT ( 'NONE', 'WORKASPACE' ) );
#12891=ORIENTED_EDGE ( 'NONE', *, *, #14032, .T. ) ;
#12905=CIRCLE ( 'NONE', #2256, 2.055000000000000160 ) ;
#12914=AXIS2_PLACEMENT_3D ( 'NONE', #5652, #4641, #9056 ) ;
#12924=EDGE_LOOP ( 'NONE', ( #12477, #4939, #7147 ) ) ;
#12925=ORIENTED_EDGE ( 'NONE', *, *, #1774, .F. ) ;
#12929=DIRECTION ( 'NONE',  ( 0.000000000000000000, 0.4999999999999993339, -0.8660254037844390407 ) ) ;
#12942=TOROIDAL_SURFACE ( 'NONE', #9199, 4.000000000000000000, 0.2500000000000000000 ) ;
#13004=LINE ( 'NONE', #8356, #5161 ) ;
#13005=VERTEX_POINT ( 'NONE', #160 ) ;
#13007=ORIENTED_EDGE ( 'NONE', *, *, #4638, .F. ) ;
#13015=ORIENTED_EDGE ( 'NONE', *, *, #7916, .F. ) ;
#13070=ORIENTED_EDGE ( 'NONE', *, *, #7014, .T. ) ;
#13118=EDGE_LOOP ( 'NONE', ( #4168, #1830, #10070, #12406 ) ) ;
#13140=ADVANCED_FACE ( 'NONE', ( #5844 ), #3742, .T. ) ;
#13166=DIRECTION ( 'NONE',  ( 1.000000000000000000, 0.000000000000000000, 0.000000000000000000 ) ) ;
#13189=VERTEX_POINT ( 'NONE', #6496 ) ;
#13292=DIRECTION ( 'NONE',  ( 0.000000000000000000, 0.5000000000000012212, 0.8660254037844380415 ) ) ;
#13323=ADVANCED_FACE ( 'NONE', ( #6782 ), #10183, .F. ) ;
#13324=ORIENTED_EDGE ( 'NONE', *, *, #8590, .T. ) ;
#13326=ORIENTED_EDGE ( 'NONE', *, *, #14111, .T. ) ;
#13339=DIRECTION ( 'NONE',  ( 1.000000000000000000, 0.000000000000000000, 0.000000000000000000 ) ) ;
#13361=VERTEX_POINT ( 'NONE', #5474 ) ;
#13368=CARTESIAN_POINT ( 'NONE',  ( 0.000000000000000000, -1.178949249685213863, 2.042000000000002924 ) ) ;
#13403=EDGE_CURVE ( 'NONE', #1625, #8017, #1392, .T. ) ;
#13456=DIRECTION ( 'NONE',  ( -1.000000000000000000, -0.000000000000000000, -0.000000000000000000 ) ) ;
#13498=CARTESIAN_POINT ( 'NONE',  ( 2.500000000000000000, 0.000000000000000000, 2.041999999999999815 ) ) ;
#13522=CARTESIAN_POINT ( 'NONE',  ( -31.74999999999995737, 0.000000000000000000, 0.000000000000000000 ) ) ;
#13556=DIRECTION ( 'NONE',  ( 0.000000000000000000, -1.000000000000000000, 0.000000000000000000 ) ) ;
#13561=CARTESIAN_POINT ( 'NONE',  ( 0.000000000000000000, -1.178949249685218303, -2.041999999999998039 ) ) ;
#13576=ORIENTED_EDGE ( 'NONE', *, *, #7991, .T. ) ;
#13625=EDGE_CURVE ( 'NONE', #3306, #9712, #12905, .T. ) ;
#13646=ORIENTED_EDGE ( 'NONE', *, *, #4556, .F. ) ;
#13649=ORIENTED_EDGE ( 'NONE', *, *, #11962, .T. ) ;
#13685=VECTOR ( 'NONE', #597, 1000.000000000000000 ) ;
#13703=ORIENTED_EDGE ( 'NONE', *, *, #4554, .F. ) ;
#13709=VERTEX_POINT ( 'NONE', #5604 ) ;
#13732=LINE ( 'NONE', #2789, #7787 ) ;
#13754=DIRECTION ( 'NONE',  ( 0.000000000000000000, 0.000000000000000000, 1.000000000000000000 ) ) ;
#13834=EDGE_CURVE ( 'NONE', #13189, #145, #3846, .T. ) ;
#13840=EDGE_CURVE ( 'NONE', #247, #6636, #6433, .T. ) ;
#13842=PLANE ( 'NONE',  #12629 ) ;
#13960=CARTESIAN_POINT ( 'NONE',  ( 2.500000000000000000, -1.178949249685213863, 2.042000000000002924 ) ) ;
#13975=EDGE_CURVE ( 'NONE', #6255, #10103, #8192, .T. ) ;
#14025=DIRECTION ( 'NONE',  ( -1.000000000000000000, -0.000000000000000000, -0.000000000000000000 ) ) ;
#14032=EDGE_CURVE ( 'NONE', #1298, #1984, #7356, .T. ) ;
#14039=AXIS2_PLACEMENT_3D ( 'NONE', #10508, #9418, #5077 ) ;
#14041=ORIENTED_EDGE ( 'NONE', *, *, #3988, .T. ) ;
#14049=AXIS2_PLACEMENT_3D ( 'NONE', #10180, #10318, #8206 ) ;
#14055=CIRCLE ( 'NONE', #10604, 2.055000000000000160 ) ;
#14111=EDGE_CURVE ( 'NONE', #6636, #2861, #819, .T. ) ;
#14175=CARTESIAN_POINT ( 'NONE',  ( 2.500000000000000000, 1.178949249685213863, -2.042000000000001148 ) ) ;
#14180=EDGE_CURVE ( 'NONE', #8184, #4062, #6887, .T. ) ;
#14188=DIRECTION ( 'NONE',  ( 0.000000000000000000, 0.000000000000000000, -1.000000000000000000 ) ) ;
#14192=CARTESIAN_POINT ( 'NONE',  ( 2.500000000000000000, -1.178949249685213863, 2.042000000000002924 ) ) ;
#14194=CARTESIAN_POINT ( 'NONE',  ( 2.500000000000000000, 2.357898499370433054, -1.951563910473907981E-15 ) ) ;
#14206=DIRECTION ( 'NONE',  ( -1.000000000000000000, -0.000000000000000000, -0.000000000000000000 ) ) ;
#14223=LINE ( 'NONE', #1153, #492 ) ;
#14272=EDGE_LOOP ( 'NONE', ( #11042, #1081, #13007, #8337, #589 ) ) ;
#14276=EDGE_CURVE ( 'NONE', #794, #568, #11237, .T. ) ;
#14288=ORIENTED_EDGE ( 'NONE', *, *, #6270, .T. ) ;
#14411=COLOUR_RGB('Black',0.12,0.14,0.17);
#14412=FILL_AREA_STYLE_COLOUR('',#14411);
#14413=FILL_AREA_STYLE('',(#14412));
#14414=SURFACE_STYLE_FILL_AREA(#14413);
#14415=SURFACE_SIDE_STYLE('',(#14414));
#14416=SURFACE_STYLE_USAGE(.BOTH.,#14415);
#14417=PRESENTATION_STYLE_ASSIGNMENT((#14416));
ENDSEC;
END-ISO-10303-21;
